ISO-10303-21;
HEADER;
/* Generated by software containing ST-Developer
 * from STEP Tools, Inc. (www.steptools.com) 
 */
/* OPTION: using custom renumber hook */

FILE_DESCRIPTION(
/* description */ ('STEP AP242 Edition 2', 'CAx-IF Rec.Pracs.---Representation and Presentation of Product Manufa
cturing Information (PMI)---4.0---2014-10-13', 'CAx-IF Rec.Pracs.---3D Tessellated Geometry---0.4---2014-09-14', '2;1', 'CAx-IF Rec.Pracs.---User Defined Attributes---1.5---2016-08-15'),
/* implementation_level */ '2;1');

FILE_NAME(
/* name */ 'binding head screw_ai_CR-BHMS 0.099-48x0.25x0.25-N.step',
/* time_stamp */ '2026-10-08T12:15:07Z',
/* author */ (''),
/* organization */ (''),
/* preprocessor_version */ 'ST-DEVELOPER v20',
/* originating_system */ 'ONSHAPE BY PTC INC, 1.221',
/* authorisation */ '  ');

FILE_SCHEMA (('AP242_MANAGED_MODEL_BASED_3D_ENGINEERING_MIM_LF { 1 0 10303 442 3 1 4 }'));
ENDSEC;

DATA;
#14=SPHERICAL_SURFACE('',#14256,0.00614054579032417);
#22=CONICAL_SURFACE('',#14259,0.0026416,0.0872664625997183);
#62=COLOUR_RGB('', 0.09019608, 0.27058824, 0.51372549);
#207=SHAPE_REPRESENTATION_RELATIONSHIP('','',#13781,#234);
#234=ADVANCED_BREP_SHAPE_REPRESENTATION('',(#13725),#45471);
#569=CIRCLE('',#14227,0.00564195203204444);
#570=CIRCLE('',#14229,0.00613648743432167);
#571=CIRCLE('',#14231,0.00613648743432167);
#572=CIRCLE('',#14233,0.00564195203204444);
#573=CIRCLE('',#14235,0.00613648743432167);
#574=CIRCLE('',#14237,0.00613648743432167);
#575=CIRCLE('',#14239,0.00564195203204444);
#576=CIRCLE('',#14241,0.00564195203204444);
#577=CIRCLE('',#14244,0.0012573);
#578=CIRCLE('',#14245,0.0026416);
#579=CIRCLE('',#14247,0.0012573);
#580=CIRCLE('',#14249,0.00613648743432167);
#581=CIRCLE('',#14251,0.00613648743432167);
#582=CIRCLE('',#14253,0.00613648743432167);
#583=CIRCLE('',#14255,0.00613648743432167);
#584=CIRCLE('',#14257,0.00255937815401834);
#1256=PLANE('',#14226);
#1257=PLANE('',#14228);
#1258=PLANE('',#14230);
#1259=PLANE('',#14232);
#1260=PLANE('',#14234);
#1261=PLANE('',#14236);
#1262=PLANE('',#14238);
#1263=PLANE('',#14240);
#1264=PLANE('',#14242);
#1265=PLANE('',#14243);
#1266=PLANE('',#14246);
#1267=PLANE('',#14248);
#1268=PLANE('',#14250);
#1269=PLANE('',#14252);
#1270=PLANE('',#14254);
#1615=CYLINDRICAL_SURFACE('',#14258,0.0012573);
#2812=ORIENTED_EDGE('',*,*,#6053,.T.);
#2813=ORIENTED_EDGE('',*,*,#6054,.T.);
#2814=ORIENTED_EDGE('',*,*,#6055,.F.);
#2815=ORIENTED_EDGE('',*,*,#6056,.F.);
#2816=ORIENTED_EDGE('',*,*,#6057,.F.);
#2817=ORIENTED_EDGE('',*,*,#6054,.F.);
#2818=ORIENTED_EDGE('',*,*,#6058,.F.);
#2819=ORIENTED_EDGE('',*,*,#6056,.T.);
#2820=ORIENTED_EDGE('',*,*,#6059,.F.);
#2821=ORIENTED_EDGE('',*,*,#6060,.F.);
#2822=ORIENTED_EDGE('',*,*,#6061,.T.);
#2823=ORIENTED_EDGE('',*,*,#6062,.T.);
#2824=ORIENTED_EDGE('',*,*,#6063,.F.);
#2825=ORIENTED_EDGE('',*,*,#6064,.F.);
#2826=ORIENTED_EDGE('',*,*,#6064,.T.);
#2827=ORIENTED_EDGE('',*,*,#6065,.F.);
#2828=ORIENTED_EDGE('',*,*,#6066,.F.);
#2829=ORIENTED_EDGE('',*,*,#6067,.F.);
#2830=ORIENTED_EDGE('',*,*,#6062,.F.);
#2831=ORIENTED_EDGE('',*,*,#6068,.F.);
#2832=ORIENTED_EDGE('',*,*,#6069,.F.);
#2833=ORIENTED_EDGE('',*,*,#6070,.T.);
#2834=ORIENTED_EDGE('',*,*,#6071,.T.);
#2835=ORIENTED_EDGE('',*,*,#6072,.F.);
#2836=ORIENTED_EDGE('',*,*,#6073,.T.);
#2837=ORIENTED_EDGE('',*,*,#6074,.T.);
#2838=ORIENTED_EDGE('',*,*,#6075,.F.);
#2839=ORIENTED_EDGE('',*,*,#6076,.F.);
#2840=ORIENTED_EDGE('',*,*,#6063,.T.);
#2841=ORIENTED_EDGE('',*,*,#6075,.T.);
#2842=ORIENTED_EDGE('',*,*,#6055,.T.);
#2843=ORIENTED_EDGE('',*,*,#6072,.T.);
#2844=ORIENTED_EDGE('',*,*,#6077,.T.);
#2845=ORIENTED_EDGE('',*,*,#6078,.F.);
#2846=ORIENTED_EDGE('',*,*,#6079,.F.);
#2847=ORIENTED_EDGE('',*,*,#6080,.F.);
#2848=ORIENTED_EDGE('',*,*,#6065,.T.);
#2849=ORIENTED_EDGE('',*,*,#6071,.F.);
#2850=ORIENTED_EDGE('',*,*,#6076,.T.);
#2851=ORIENTED_EDGE('',*,*,#6067,.T.);
#2852=ORIENTED_EDGE('',*,*,#6081,.F.);
#2853=ORIENTED_EDGE('',*,*,#6069,.T.);
#2854=ORIENTED_EDGE('',*,*,#6057,.T.);
#2855=ORIENTED_EDGE('',*,*,#6082,.F.);
#2856=ORIENTED_EDGE('',*,*,#6083,.F.);
#2857=ORIENTED_EDGE('',*,*,#6059,.T.);
#2858=ORIENTED_EDGE('',*,*,#6074,.F.);
#2859=ORIENTED_EDGE('',*,*,#6070,.F.);
#2860=ORIENTED_EDGE('',*,*,#6082,.T.);
#2861=ORIENTED_EDGE('',*,*,#6058,.T.);
#2862=ORIENTED_EDGE('',*,*,#6053,.F.);
#2863=ORIENTED_EDGE('',*,*,#6060,.T.);
#2864=ORIENTED_EDGE('',*,*,#6083,.T.);
#2865=ORIENTED_EDGE('',*,*,#6073,.F.);
#2866=ORIENTED_EDGE('',*,*,#6081,.T.);
#2867=ORIENTED_EDGE('',*,*,#6068,.T.);
#2868=ORIENTED_EDGE('',*,*,#6061,.F.);
#2869=ORIENTED_EDGE('',*,*,#6066,.T.);
#2870=ORIENTED_EDGE('',*,*,#6080,.T.);
#2871=ORIENTED_EDGE('',*,*,#6084,.T.);
#2872=ORIENTED_EDGE('',*,*,#6077,.F.);
#2873=ORIENTED_EDGE('',*,*,#6079,.T.);
#2874=ORIENTED_EDGE('',*,*,#6078,.T.);
#2875=ORIENTED_EDGE('',*,*,#6084,.F.);
#6053=EDGE_CURVE('',#7765,#7766,#569,.T.);
#6054=EDGE_CURVE('',#7766,#7767,#8876,.T.);
#6055=EDGE_CURVE('',#7768,#7767,#8877,.T.);
#6056=EDGE_CURVE('',#7765,#7768,#8878,.T.);
#6057=EDGE_CURVE('',#7767,#7769,#8879,.T.);
#6058=EDGE_CURVE('',#7769,#7766,#570,.T.);
#6059=EDGE_CURVE('',#7770,#7768,#8880,.T.);
#6060=EDGE_CURVE('',#7765,#7770,#571,.T.);
#6061=EDGE_CURVE('',#7771,#7772,#572,.T.);
#6062=EDGE_CURVE('',#7772,#7773,#8881,.T.);
#6063=EDGE_CURVE('',#7774,#7773,#8882,.T.);
#6064=EDGE_CURVE('',#7771,#7774,#8883,.T.);
#6065=EDGE_CURVE('',#7775,#7774,#8884,.T.);
#6066=EDGE_CURVE('',#7771,#7775,#573,.T.);
#6067=EDGE_CURVE('',#7773,#7776,#8885,.T.);
#6068=EDGE_CURVE('',#7776,#7772,#574,.T.);
#6069=EDGE_CURVE('',#7777,#7767,#8886,.T.);
#6070=EDGE_CURVE('',#7777,#7778,#575,.T.);
#6071=EDGE_CURVE('',#7778,#7774,#8887,.T.);
#6072=EDGE_CURVE('',#7767,#7774,#8888,.T.);
#6073=EDGE_CURVE('',#7779,#7780,#576,.T.);
#6074=EDGE_CURVE('',#7780,#7768,#8889,.T.);
#6075=EDGE_CURVE('',#7773,#7768,#8890,.T.);
#6076=EDGE_CURVE('',#7779,#7773,#8891,.T.);
#6077=EDGE_CURVE('',#7781,#7781,#577,.T.);
#6078=EDGE_CURVE('',#7782,#7782,#578,.T.);
#6079=EDGE_CURVE('',#7783,#7783,#579,.T.);
#6080=EDGE_CURVE('',#7775,#7778,#580,.T.);
#6081=EDGE_CURVE('',#7779,#7776,#581,.T.);
#6082=EDGE_CURVE('',#7777,#7769,#582,.T.);
#6083=EDGE_CURVE('',#7770,#7780,#583,.T.);
#6084=EDGE_CURVE('',#7784,#7784,#584,.T.);
#7765=VERTEX_POINT('',#31595);
#7766=VERTEX_POINT('',#31596);
#7767=VERTEX_POINT('',#31598);
#7768=VERTEX_POINT('',#31600);
#7769=VERTEX_POINT('',#31604);
#7770=VERTEX_POINT('',#31608);
#7771=VERTEX_POINT('',#31612);
#7772=VERTEX_POINT('',#31613);
#7773=VERTEX_POINT('',#31615);
#7774=VERTEX_POINT('',#31617);
#7775=VERTEX_POINT('',#31621);
#7776=VERTEX_POINT('',#31625);
#7777=VERTEX_POINT('',#31629);
#7778=VERTEX_POINT('',#31631);
#7779=VERTEX_POINT('',#31636);
#7780=VERTEX_POINT('',#31637);
#7781=VERTEX_POINT('',#31644);
#7782=VERTEX_POINT('',#31646);
#7783=VERTEX_POINT('',#31649);
#7784=VERTEX_POINT('',#31660);
#8876=LINE('',#31597,#9704);
#8877=LINE('',#31599,#9705);
#8878=LINE('',#31601,#9706);
#8879=LINE('',#31603,#9707);
#8880=LINE('',#31607,#9708);
#8881=LINE('',#31614,#9709);
#8882=LINE('',#31616,#9710);
#8883=LINE('',#31618,#9711);
#8884=LINE('',#31620,#9712);
#8885=LINE('',#31624,#9713);
#8886=LINE('',#31628,#9714);
#8887=LINE('',#31632,#9715);
#8888=LINE('',#31633,#9716);
#8889=LINE('',#31638,#9717);
#8890=LINE('',#31639,#9718);
#8891=LINE('',#31640,#9719);
#9704=VECTOR('',#16250,1.);
#9705=VECTOR('',#16251,1.);
#9706=VECTOR('',#16252,1.);
#9707=VECTOR('',#16255,1.);
#9708=VECTOR('',#16260,1.);
#9709=VECTOR('',#16267,1.);
#9710=VECTOR('',#16268,1.);
#9711=VECTOR('',#16269,1.);
#9712=VECTOR('',#16272,1.);
#9713=VECTOR('',#16277,1.);
#9714=VECTOR('',#16282,1.);
#9715=VECTOR('',#16285,1.);
#9716=VECTOR('',#16286,1.);
#9717=VECTOR('',#16291,1.);
#9718=VECTOR('',#16292,1.);
#9719=VECTOR('',#16293,1.);
#10755=EDGE_LOOP('',(#2812,#2813,#2814,#2815));
#10756=EDGE_LOOP('',(#2816,#2817,#2818));
#10757=EDGE_LOOP('',(#2819,#2820,#2821));
#10758=EDGE_LOOP('',(#2822,#2823,#2824,#2825));
#10759=EDGE_LOOP('',(#2826,#2827,#2828));
#10760=EDGE_LOOP('',(#2829,#2830,#2831));
#10761=EDGE_LOOP('',(#2832,#2833,#2834,#2835));
#10762=EDGE_LOOP('',(#2836,#2837,#2838,#2839));
#10763=EDGE_LOOP('',(#2840,#2841,#2842,#2843));
#10764=EDGE_LOOP('',(#2844));
#10765=EDGE_LOOP('',(#2845));
#10766=EDGE_LOOP('',(#2846));
#10767=EDGE_LOOP('',(#2847,#2848,#2849));
#10768=EDGE_LOOP('',(#2850,#2851,#2852));
#10769=EDGE_LOOP('',(#2853,#2854,#2855));
#10770=EDGE_LOOP('',(#2856,#2857,#2858));
#10771=EDGE_LOOP('',(#2859,#2860,#2861,#2862,#2863,#2864,#2865,#2866,#2867,
#2868,#2869,#2870));
#10772=EDGE_LOOP('',(#2871));
#10773=EDGE_LOOP('',(#2872));
#10774=EDGE_LOOP('',(#2873));
#10775=EDGE_LOOP('',(#2874));
#10776=EDGE_LOOP('',(#2875));
#11870=FACE_BOUND('',#10755,.T.);
#11871=FACE_BOUND('',#10756,.T.);
#11872=FACE_BOUND('',#10757,.T.);
#11873=FACE_BOUND('',#10758,.T.);
#11874=FACE_BOUND('',#10759,.T.);
#11875=FACE_BOUND('',#10760,.T.);
#11876=FACE_BOUND('',#10761,.T.);
#11877=FACE_BOUND('',#10762,.T.);
#11878=FACE_BOUND('',#10763,.T.);
#11879=FACE_BOUND('',#10764,.T.);
#11880=FACE_BOUND('',#10765,.T.);
#11881=FACE_BOUND('',#10766,.T.);
#11882=FACE_BOUND('',#10767,.T.);
#11883=FACE_BOUND('',#10768,.T.);
#11884=FACE_BOUND('',#10769,.T.);
#11885=FACE_BOUND('',#10770,.T.);
#11886=FACE_BOUND('',#10771,.T.);
#11887=FACE_BOUND('',#10772,.T.);
#11888=FACE_BOUND('',#10773,.T.);
#11889=FACE_BOUND('',#10774,.T.);
#11890=FACE_BOUND('',#10775,.T.);
#11891=FACE_BOUND('',#10776,.T.);
#12918=ADVANCED_FACE('',(#11870),#1256,.F.);
#12919=ADVANCED_FACE('',(#11871),#1257,.T.);
#12920=ADVANCED_FACE('',(#11872),#1258,.T.);
#12921=ADVANCED_FACE('',(#11873),#1259,.F.);
#12922=ADVANCED_FACE('',(#11874),#1260,.T.);
#12923=ADVANCED_FACE('',(#11875),#1261,.T.);
#12924=ADVANCED_FACE('',(#11876),#1262,.F.);
#12925=ADVANCED_FACE('',(#11877),#1263,.F.);
#12926=ADVANCED_FACE('',(#11878),#1264,.T.);
#12927=ADVANCED_FACE('',(#11879,#11880),#1265,.F.);
#12928=ADVANCED_FACE('',(#11881),#1266,.T.);
#12929=ADVANCED_FACE('',(#11882),#1267,.T.);
#12930=ADVANCED_FACE('',(#11883),#1268,.T.);
#12931=ADVANCED_FACE('',(#11884),#1269,.T.);
#12932=ADVANCED_FACE('',(#11885),#1270,.T.);
#12933=ADVANCED_FACE('',(#11886,#11887),#14,.T.);
#12934=ADVANCED_FACE('',(#11888,#11889),#1615,.T.);
#12935=ADVANCED_FACE('',(#11890,#11891),#22,.T.);
#13508=CLOSED_SHELL('',(#12918,#12919,#12920,#12921,#12922,#12923,#12924,
#12925,#12926,#12927,#12928,#12929,#12930,#12931,#12932,#12933,#12934,#12935));
#13535=STYLED_ITEM('',(#13562),#13725);
#13562=PRESENTATION_STYLE_ASSIGNMENT((#13589));
#13589=SURFACE_STYLE_USAGE(.BOTH.,#13616);
#13616=SURFACE_SIDE_STYLE('',(#13643));
#13643=SURFACE_STYLE_FILL_AREA(#13670);
#13670=FILL_AREA_STYLE('',(#13697));
#13697=FILL_AREA_STYLE_COLOUR('',#62);
#13725=MANIFOLD_SOLID_BREP(
'binding head screw_ai_CR-BHMS 0.099-48x0.25x0.25-N',#13508);
#13753=SHAPE_DEFINITION_REPRESENTATION(#45536,#13781);
#13781=SHAPE_REPRESENTATION(
'binding head screw_ai_CR-BHMS 0.099-48x0.25x0.25-N',(#13802),#45471);
#13802=AXIS2_PLACEMENT_3D('',#19109,#15295,#15296);
#14226=AXIS2_PLACEMENT_3D('',#31593,#16246,#16247);
#14227=AXIS2_PLACEMENT_3D('',#31594,#16248,#16249);
#14228=AXIS2_PLACEMENT_3D('',#31602,#16253,#16254);
#14229=AXIS2_PLACEMENT_3D('',#31605,#16256,#16257);
#14230=AXIS2_PLACEMENT_3D('',#31606,#16258,#16259);
#14231=AXIS2_PLACEMENT_3D('',#31609,#16261,#16262);
#14232=AXIS2_PLACEMENT_3D('',#31610,#16263,#16264);
#14233=AXIS2_PLACEMENT_3D('',#31611,#16265,#16266);
#14234=AXIS2_PLACEMENT_3D('',#31619,#16270,#16271);
#14235=AXIS2_PLACEMENT_3D('',#31622,#16273,#16274);
#14236=AXIS2_PLACEMENT_3D('',#31623,#16275,#16276);
#14237=AXIS2_PLACEMENT_3D('',#31626,#16278,#16279);
#14238=AXIS2_PLACEMENT_3D('',#31627,#16280,#16281);
#14239=AXIS2_PLACEMENT_3D('',#31630,#16283,#16284);
#14240=AXIS2_PLACEMENT_3D('',#31634,#16287,#16288);
#14241=AXIS2_PLACEMENT_3D('',#31635,#16289,#16290);
#14242=AXIS2_PLACEMENT_3D('',#31641,#16294,#16295);
#14243=AXIS2_PLACEMENT_3D('',#31642,#16296,#16297);
#14244=AXIS2_PLACEMENT_3D('',#31643,#16298,#16299);
#14245=AXIS2_PLACEMENT_3D('',#31645,#16300,#16301);
#14246=AXIS2_PLACEMENT_3D('',#31647,#16302,#16303);
#14247=AXIS2_PLACEMENT_3D('',#31648,#16304,#16305);
#14248=AXIS2_PLACEMENT_3D('',#31650,#16306,#16307);
#14249=AXIS2_PLACEMENT_3D('',#31651,#16308,#16309);
#14250=AXIS2_PLACEMENT_3D('',#31652,#16310,#16311);
#14251=AXIS2_PLACEMENT_3D('',#31653,#16312,#16313);
#14252=AXIS2_PLACEMENT_3D('',#31654,#16314,#16315);
#14253=AXIS2_PLACEMENT_3D('',#31655,#16316,#16317);
#14254=AXIS2_PLACEMENT_3D('',#31656,#16318,#16319);
#14255=AXIS2_PLACEMENT_3D('',#31657,#16320,#16321);
#14256=AXIS2_PLACEMENT_3D('',#31658,#16322,#16323);
#14257=AXIS2_PLACEMENT_3D('',#31659,#16324,#16325);
#14258=AXIS2_PLACEMENT_3D('',#31661,#16326,#16327);
#14259=AXIS2_PLACEMENT_3D('',#31662,#16328,#16329);
#15295=DIRECTION('',(0.,0.,1.));
#15296=DIRECTION('',(1.,0.,0.));
#16246=DIRECTION('',(0.616239312964626,2.85818950259745E-15,-0.787558955987986));
#16247=DIRECTION('',(0.787558955987986,-2.15158806147751E-15,0.616239312964626));
#16248=DIRECTION('',(-0.616239312964626,-2.85818950259745E-15,0.787558955987986));
#16249=DIRECTION('',(-0.787558955987986,0.,-0.616239312964626));
#16250=DIRECTION('',(0.785096318706608,0.0790194346750136,0.614312379247703));
#16251=DIRECTION('',(0.,-1.,-1.37693951293562E-16));
#16252=DIRECTION('',(0.785096318706608,-0.079019434675018,0.614312379247703));
#16253=DIRECTION('',(-0.100143387937821,0.994973015640291,3.47392971676056E-15));
#16254=DIRECTION('',(-0.994973015640291,-0.100143387937821,-3.49648770193432E-16));
#16255=DIRECTION('',(-0.990021088684022,-0.0996449797052097,-0.0996449797052101));
#16256=DIRECTION('',(0.100143387937821,-0.994973015640291,-3.47392971676056E-15));
#16257=DIRECTION('',(-0.994973015640291,-0.100143387937821,0.));
#16258=DIRECTION('',(-0.100143387937822,-0.994973015640291,-3.59560665342334E-15));
#16259=DIRECTION('',(0.994973015640291,-0.100143387937822,-3.49648770193432E-16));
#16260=DIRECTION('',(0.990021088684022,-0.0996449797052105,0.0996449797052101));
#16261=DIRECTION('',(0.100143387937822,0.994973015640291,3.59560665342334E-15));
#16262=DIRECTION('',(0.994973015640291,-0.100143387937822,0.));
#16263=DIRECTION('',(0.616239312964626,-2.74974739807084E-15,0.787558955987986));
#16264=DIRECTION('',(-0.787558955987986,-2.15158806147751E-15,0.616239312964626));
#16265=DIRECTION('',(-0.616239312964626,2.74974739807084E-15,-0.787558955987986));
#16266=DIRECTION('',(0.787558955987986,1.06581410364015E-14,-0.616239312964626));
#16267=DIRECTION('',(0.785096318706608,-0.0790194346750135,-0.614312379247703));
#16268=DIRECTION('',(0.,1.,6.88469756467808E-17));
#16269=DIRECTION('',(0.785096318706608,0.0790194346750179,-0.614312379247703));
#16270=DIRECTION('',(-0.100143387937821,0.994973015640291,3.47392971676056E-15));
#16271=DIRECTION('',(-0.994973015640291,-0.100143387937821,-3.49648770193432E-16));
#16272=DIRECTION('',(0.990021088684022,0.0996449797052104,-0.09964497970521));
#16273=DIRECTION('',(0.100143387937821,-0.994973015640291,-3.47392971676056E-15));
#16274=DIRECTION('',(-0.994973015640291,-0.100143387937821,-9.76996261670138E-15));
#16275=DIRECTION('',(-0.100143387937822,-0.994973015640291,-3.59560665342334E-15));
#16276=DIRECTION('',(0.994973015640291,-0.100143387937822,-3.49648770193432E-16));
#16277=DIRECTION('',(-0.990021088684022,0.0996449797052097,0.09964497970521));
#16278=DIRECTION('',(0.100143387937822,0.994973015640291,3.59560665342334E-15));
#16279=DIRECTION('',(0.994973015640291,-0.100143387937822,0.));
#16280=DIRECTION('',(0.616239312964626,-0.787558955987986,-1.08442104526618E-16));
#16281=DIRECTION('',(0.787558955987986,0.616239312964626,0.));
#16282=DIRECTION('',(0.785096318706608,0.614312379247703,0.0790194346750159));
#16283=DIRECTION('',(-0.616239312964626,0.787558955987986,1.08442104526618E-16));
#16284=DIRECTION('',(0.787558955987986,0.616239312964626,0.));
#16285=DIRECTION('',(0.785096318706608,0.614312379247703,-0.0790194346750157));
#16286=DIRECTION('',(0.,-1.37693951293562E-16,1.));
#16287=DIRECTION('',(0.616239312964626,0.787558955987986,0.));
#16288=DIRECTION('',(-0.787558955987986,0.616239312964626,0.));
#16289=DIRECTION('',(-0.616239312964626,-0.787558955987986,0.));
#16290=DIRECTION('',(-0.787558955987986,0.616239312964626,3.19744231092045E-14));
#16291=DIRECTION('',(0.785096318706608,-0.614312379247703,0.0790194346750157));
#16292=DIRECTION('',(0.,0.,-1.));
#16293=DIRECTION('',(0.785096318706608,-0.614312379247703,-0.0790194346750157));
#16294=DIRECTION('',(-1.,0.,0.));
#16295=DIRECTION('',(0.,0.,1.));
#16296=DIRECTION('',(-1.,0.,0.));
#16297=DIRECTION('',(0.,0.,1.));
#16298=DIRECTION('',(-1.,0.,0.));
#16299=DIRECTION('',(0.,0.,1.));
#16300=DIRECTION('',(-1.,0.,0.));
#16301=DIRECTION('',(0.,0.,1.));
#16302=DIRECTION('',(1.,0.,0.));
#16303=DIRECTION('',(0.,0.,-1.));
#16304=DIRECTION('',(-1.,0.,0.));
#16305=DIRECTION('',(0.,0.,1.));
#16306=DIRECTION('',(-0.100143387937821,0.,-0.994973015640291));
#16307=DIRECTION('',(-0.994973015640291,0.,0.100143387937821));
#16308=DIRECTION('',(0.100143387937821,0.,0.994973015640291));
#16309=DIRECTION('',(-0.994973015640291,0.,0.100143387937821));
#16310=DIRECTION('',(-0.100143387937821,0.,-0.994973015640291));
#16311=DIRECTION('',(-0.994973015640291,0.,0.100143387937821));
#16312=DIRECTION('',(0.100143387937821,0.,0.994973015640291));
#16313=DIRECTION('',(-0.994973015640291,2.66453525910038E-15,0.100143387937821));
#16314=DIRECTION('',(-0.100143387937822,-1.21676936662784E-16,0.994973015640291));
#16315=DIRECTION('',(0.994973015640291,0.,0.100143387937822));
#16316=DIRECTION('',(0.100143387937822,1.21676936662784E-16,-0.994973015640291));
#16317=DIRECTION('',(0.994973015640291,0.,0.100143387937822));
#16318=DIRECTION('',(-0.100143387937822,-1.21676936662784E-16,0.994973015640291));
#16319=DIRECTION('',(0.994973015640291,0.,0.100143387937822));
#16320=DIRECTION('',(0.100143387937822,1.21676936662784E-16,-0.994973015640291));
#16321=DIRECTION('',(0.994973015640291,0.,0.100143387937822));
#16322=DIRECTION('',(0.,0.,1.));
#16323=DIRECTION('',(0.,-1.,0.));
#16324=DIRECTION('',(-1.,0.,0.));
#16325=DIRECTION('',(0.,0.,1.));
#16326=DIRECTION('',(-1.,0.,0.));
#16327=DIRECTION('',(0.,0.,1.));
#16328=DIRECTION('',(1.,0.,0.));
#16329=DIRECTION('',(0.,0.,-1.));
#19109=CARTESIAN_POINT('',(0.,0.,0.));
#31593=CARTESIAN_POINT('',(0.0019558,0.00019685,-0.00019685));
#31594=CARTESIAN_POINT('',(0.00464692103339967,-6.71076465535595E-18,0.00190886483457572));
#31595=CARTESIAN_POINT('',(0.000213232602987236,0.000372238276972069,-0.00156035241129895));
#31596=CARTESIAN_POINT('',(0.000213232602987236,-0.000372238276972058,-0.00156035241129895));
#31597=CARTESIAN_POINT('',(0.,-0.000393699999999994,-0.0017272));
#31598=CARTESIAN_POINT('',(0.0019558,-0.00019685,-0.00019685));
#31599=CARTESIAN_POINT('',(0.0019558,0.00019685,-0.00019685));
#31600=CARTESIAN_POINT('',(0.0019558,0.00019685,-0.00019685));
#31601=CARTESIAN_POINT('',(0.,0.000393700000000006,-0.0017272));
#31602=CARTESIAN_POINT('',(0.00220737593360996,-0.000171529045643153,-5.98890461932643E-19));
#31603=CARTESIAN_POINT('',(0.00222429738224716,-0.000169825912825772,-0.000169825912825772));
#31604=CARTESIAN_POINT('',(2.49715212940994E-5,-0.000391186632597021,-0.000391186632597022));
#31605=CARTESIAN_POINT('',(0.0061181923658055,0.000222092088766138,7.75430383431664E-19));
#31606=CARTESIAN_POINT('',(0.00220737593360996,0.000171529045643153,5.98890461932643E-19));
#31607=CARTESIAN_POINT('',(0.00222429738224716,0.000169825912825773,-0.000169825912825772));
#31608=CARTESIAN_POINT('',(2.49715212940986E-5,0.000391186632597024,-0.000391186632597022));
#31609=CARTESIAN_POINT('',(0.0061181923658055,-0.000222092088766138,-8.02590401435484E-19));
#31610=CARTESIAN_POINT('',(0.0019558,-0.00019685,0.00019685));
#31611=CARTESIAN_POINT('',(0.00464692103339967,6.88160638279209E-18,-0.00190886483457572));
#31612=CARTESIAN_POINT('',(0.000213232602987235,-0.000372238276972069,0.00156035241129894));
#31613=CARTESIAN_POINT('',(0.000213232602987237,0.000372238276972058,0.00156035241129895));
#31614=CARTESIAN_POINT('',(0.,0.000393699999999994,0.0017272));
#31615=CARTESIAN_POINT('',(0.0019558,0.00019685,0.00019685));
#31616=CARTESIAN_POINT('',(0.0019558,-0.00019685,0.00019685));
#31617=CARTESIAN_POINT('',(0.0019558,-0.00019685,0.00019685));
#31618=CARTESIAN_POINT('',(0.,-0.000393700000000006,0.0017272));
#31619=CARTESIAN_POINT('',(0.00220737593360996,-0.000171529045643153,-5.98890461932643E-19));
#31620=CARTESIAN_POINT('',(0.00222429738224716,-0.000169825912825773,0.000169825912825772));
#31621=CARTESIAN_POINT('',(2.49715212940986E-5,-0.000391186632597024,0.000391186632597022));
#31622=CARTESIAN_POINT('',(0.0061181923658055,0.000222092088766138,7.75430383431664E-19));
#31623=CARTESIAN_POINT('',(0.00220737593360996,0.000171529045643153,5.98890461932643E-19));
#31624=CARTESIAN_POINT('',(0.00222429738224716,0.000169825912825772,0.000169825912825772));
#31625=CARTESIAN_POINT('',(2.49715212940994E-5,0.000391186632597021,0.000391186632597022));
#31626=CARTESIAN_POINT('',(0.0061181923658055,-0.000222092088766138,-8.02590401435484E-19));
#31627=CARTESIAN_POINT('',(0.0019558,-0.00019685,-0.00019685));
#31628=CARTESIAN_POINT('',(0.,-0.0017272,-0.0003937));
#31629=CARTESIAN_POINT('',(0.000213232602987236,-0.00156035241129895,-0.000372238276972064));
#31630=CARTESIAN_POINT('',(0.00464692103339967,0.00190886483457572,2.62839141558061E-19));
#31631=CARTESIAN_POINT('',(0.000213232602987236,-0.00156035241129895,0.000372238276972064));
#31632=CARTESIAN_POINT('',(0.,-0.0017272,0.0003937));
#31633=CARTESIAN_POINT('',(0.0019558,-0.00019685,-0.00019685));
#31634=CARTESIAN_POINT('',(0.0019558,0.00019685,0.00019685));
#31635=CARTESIAN_POINT('',(0.00464692103339967,-0.00190886483457572,0.));
#31636=CARTESIAN_POINT('',(0.000213232602987235,0.00156035241129895,0.000372238276972064));
#31637=CARTESIAN_POINT('',(0.000213232602987235,0.00156035241129895,-0.000372238276972064));
#31638=CARTESIAN_POINT('',(0.,0.0017272,-0.0003937));
#31639=CARTESIAN_POINT('',(0.0019558,0.00019685,0.00019685));
#31640=CARTESIAN_POINT('',(0.,0.0017272,0.0003937));
#31641=CARTESIAN_POINT('',(0.0019558,0.00019685,0.00019685));
#31642=CARTESIAN_POINT('',(0.0014986,0.0012573,0.));
#31643=CARTESIAN_POINT('',(0.0014986,0.,0.));
#31644=CARTESIAN_POINT('',(0.0014986,0.,0.0012573));
#31645=CARTESIAN_POINT('',(0.0014986,0.,0.));
#31646=CARTESIAN_POINT('',(0.0014986,0.,0.0026416));
#31647=CARTESIAN_POINT('',(0.0078486,0.0012573,0.));
#31648=CARTESIAN_POINT('',(0.0078486,0.,0.));
#31649=CARTESIAN_POINT('',(0.0078486,0.,0.0012573));
#31650=CARTESIAN_POINT('',(0.00220737593360996,0.,0.000171529045643153));
#31651=CARTESIAN_POINT('',(0.0061181923658055,2.16840434497101E-19,-0.000222092088766138));
#31652=CARTESIAN_POINT('',(0.00220737593360996,0.,0.000171529045643153));
#31653=CARTESIAN_POINT('',(0.0061181923658055,2.16840434497101E-19,-0.000222092088766138));
#31654=CARTESIAN_POINT('',(0.00220737593360996,0.,-0.000171529045643153));
#31655=CARTESIAN_POINT('',(0.0061181923658055,1.89680416493284E-19,0.000222092088766138));
#31656=CARTESIAN_POINT('',(0.00220737593360996,0.,-0.000171529045643153));
#31657=CARTESIAN_POINT('',(0.0061181923658055,1.89680416493284E-19,0.000222092088766138));
#31658=CARTESIAN_POINT('',(0.00614054579032417,2.16840434497101E-19,0.));
#31659=CARTESIAN_POINT('',(0.0005588,0.,0.));
#31660=CARTESIAN_POINT('',(0.0005588,0.,0.00255937815401834));
#31661=CARTESIAN_POINT('',(-0.0254,0.,0.));
#31662=CARTESIAN_POINT('',(0.0014986,0.,0.));
#45463=MECHANICAL_DESIGN_GEOMETRIC_PRESENTATION_REPRESENTATION('',(#13535),#45464);
#45464=(
GEOMETRIC_REPRESENTATION_CONTEXT(3)
GLOBAL_UNCERTAINTY_ASSIGNED_CONTEXT((#45492))
GLOBAL_UNIT_ASSIGNED_CONTEXT((#45522,#45521,#45520))
REPRESENTATION_CONTEXT('MAS-690','TOP_LEVEL_ASSEMBLY_PART')
);
#45471=(
GEOMETRIC_REPRESENTATION_CONTEXT(3)
GLOBAL_UNCERTAINTY_ASSIGNED_CONTEXT((#45499))
GLOBAL_UNIT_ASSIGNED_CONTEXT((#45522,#45521,#45520))
REPRESENTATION_CONTEXT(
'binding head screw_ai_CR-BHMS 0.099-48x0.25x0.25-N','COMPONENT_PART')
);
#45492=UNCERTAINTY_MEASURE_WITH_UNIT(LENGTH_MEASURE(1.E-8),#45522,
'DISTANCE_ACCURACY_VALUE','Maximum Tolerance applied to model');
#45499=UNCERTAINTY_MEASURE_WITH_UNIT(LENGTH_MEASURE(1.E-6),#45522,
'DISTANCE_ACCURACY_VALUE','Maximum Tolerance applied to model');
#45520=(
NAMED_UNIT(*)
SI_UNIT($,.STERADIAN.)
SOLID_ANGLE_UNIT()
);
#45521=(
NAMED_UNIT(*)
PLANE_ANGLE_UNIT()
SI_UNIT($,.RADIAN.)
);
#45522=(
LENGTH_UNIT()
NAMED_UNIT(*)
SI_UNIT($,.METRE.)
);
#45536=PRODUCT_DEFINITION_SHAPE('','',#45592);
#45592=PRODUCT_DEFINITION('','',#45648,#45620);
#45620=PRODUCT_DEFINITION_CONTEXT('',#45782,'design');
#45648=PRODUCT_DEFINITION_FORMATION_WITH_SPECIFIED_SOURCE('','',#45704,
 .NOT_KNOWN.);
#45704=PRODUCT('binding head screw_ai_CR-BHMS 0.099-48x0.25x0.25-N',
'binding head screw_ai_CR-BHMS 0.099-48x0.25x0.25-N',
'binding head screw_ai_CR-BHMS 0.099-48x0.25x0.25-N',(#45760));
#45760=PRODUCT_CONTEXT('',#45782,'mechanical');
#45782=APPLICATION_CONTEXT('managed model based 3d engineering');
ENDSEC;
END-ISO-10303-21;
